ISO-10303-21;
HEADER;
/* Generated by software containing ST-Developer
 * from STEP Tools, Inc. (www.steptools.com) 
 */

FILE_DESCRIPTION(
/* description */ ('PAT-054'),
/* implementation_level */ '2;1');

FILE_NAME(
/* name */ 'Slot Nut - M5 for 20 mm Extrusion.step',
/* time_stamp */ '2026-10-29T16:38:13-07:00',
/* author */ (''),
/* organization */ (''),
/* preprocessor_version */ 'ST-DEVELOPER v20.2',
/* originating_system */ 'Autodesk Translation Framework v15.17.0.0',
/* authorisation */ '');

FILE_SCHEMA (('AUTOMOTIVE_DESIGN { 1 0 10303 214 3 1 1 }'));
ENDSEC;

DATA;
#10=MECHANICAL_DESIGN_GEOMETRIC_PRESENTATION_REPRESENTATION('',(#934),#33981);
#25=ELLIPSE('',#14185,0.299389011154384,0.2117);
#26=ELLIPSE('',#14190,0.299389011154384,0.2117);
#831=SHAPE_REPRESENTATION_RELATIONSHIP('SRR','None',#34206,#875);
#875=ADVANCED_BREP_SHAPE_REPRESENTATION('',(#993),#33954);
#934=STYLED_ITEM('',(#34524),#993);
#993=MANIFOLD_SOLID_BREP('Body1',#13045);
#1148=FACE_BOUND('',#2743,.T.);
#1390=PLANE('',#14184);
#1391=PLANE('',#14192);
#1392=PLANE('',#14193);
#1393=PLANE('',#14194);
#1394=PLANE('',#14195);
#1395=PLANE('',#14196);
#1396=PLANE('',#14197);
#1397=PLANE('',#14198);
#1398=PLANE('',#14199);
#1874=FACE_OUTER_BOUND('',#2733,.T.);
#1875=FACE_OUTER_BOUND('',#2734,.T.);
#1876=FACE_OUTER_BOUND('',#2735,.T.);
#1877=FACE_OUTER_BOUND('',#2736,.T.);
#1878=FACE_OUTER_BOUND('',#2737,.T.);
#1879=FACE_OUTER_BOUND('',#2738,.T.);
#1880=FACE_OUTER_BOUND('',#2739,.T.);
#1881=FACE_OUTER_BOUND('',#2740,.T.);
#1882=FACE_OUTER_BOUND('',#2741,.T.);
#1883=FACE_OUTER_BOUND('',#2742,.T.);
#2733=EDGE_LOOP('',(#9907,#9908,#9909,#9910,#9911,#9912));
#2734=EDGE_LOOP('',(#9913,#9914,#9915,#9916,#9917,#9918,#9919,#9920));
#2735=EDGE_LOOP('',(#9921,#9922,#9923,#9924,#9925));
#2736=EDGE_LOOP('',(#9926,#9927,#9928,#9929));
#2737=EDGE_LOOP('',(#9930,#9931,#9932,#9933,#9934,#9935));
#2738=EDGE_LOOP('',(#9936,#9937,#9938,#9939,#9940,#9941));
#2739=EDGE_LOOP('',(#9942,#9943,#9944,#9945));
#2740=EDGE_LOOP('',(#9946,#9947,#9948,#9949));
#2741=EDGE_LOOP('',(#9950,#9951,#9952,#9953,#9954,#9955));
#2742=EDGE_LOOP('',(#9956,#9957,#9958,#9959));
#2743=EDGE_LOOP('',(#9960));
#3623=LINE('',#20654,#4557);
#3624=LINE('',#20656,#4558);
#3625=LINE('',#20658,#4559);
#3626=LINE('',#20660,#4560);
#3627=LINE('',#20663,#4561);
#3628=LINE('',#20668,#4562);
#3629=LINE('',#20677,#4563);
#3630=LINE('',#20678,#4564);
#3631=LINE('',#20681,#4565);
#3632=LINE('',#20682,#4566);
#3633=LINE('',#20685,#4567);
#3634=LINE('',#20687,#4568);
#3635=LINE('',#20688,#4569);
#3636=LINE('',#20691,#4570);
#3637=LINE('',#20693,#4571);
#3638=LINE('',#20694,#4572);
#3639=LINE('',#20697,#4573);
#3640=LINE('',#20698,#4574);
#3641=LINE('',#20701,#4575);
#3642=LINE('',#20702,#4576);
#3643=LINE('',#20704,#4577);
#4557=VECTOR('',#16528,1.);
#4558=VECTOR('',#16529,1.);
#4559=VECTOR('',#16530,1.);
#4560=VECTOR('',#16531,1.);
#4561=VECTOR('',#16534,1.);
#4562=VECTOR('',#16539,0.21);
#4563=VECTOR('',#16550,1.);
#4564=VECTOR('',#16551,1.);
#4565=VECTOR('',#16554,1.);
#4566=VECTOR('',#16555,1.);
#4567=VECTOR('',#16558,1.);
#4568=VECTOR('',#16559,1.);
#4569=VECTOR('',#16560,1.);
#4570=VECTOR('',#16563,1.);
#4571=VECTOR('',#16564,1.);
#4572=VECTOR('',#16565,1.);
#4573=VECTOR('',#16568,1.);
#4574=VECTOR('',#16569,1.);
#4575=VECTOR('',#16572,1.);
#4576=VECTOR('',#16573,1.);
#4577=VECTOR('',#16576,1.);
#5396=CIRCLE('',#14187,0.2117);
#5397=CIRCLE('',#14188,0.2117);
#5398=CIRCLE('',#14189,0.2117);
#5399=CIRCLE('',#14191,0.2117);
#6060=VERTEX_POINT('',#20652);
#6061=VERTEX_POINT('',#20653);
#6062=VERTEX_POINT('',#20655);
#6063=VERTEX_POINT('',#20657);
#6064=VERTEX_POINT('',#20659);
#6065=VERTEX_POINT('',#20661);
#6066=VERTEX_POINT('',#20665);
#6067=VERTEX_POINT('',#20667);
#6068=VERTEX_POINT('',#20670);
#6069=VERTEX_POINT('',#20672);
#6070=VERTEX_POINT('',#20676);
#6071=VERTEX_POINT('',#20680);
#6072=VERTEX_POINT('',#20684);
#6073=VERTEX_POINT('',#20686);
#6074=VERTEX_POINT('',#20690);
#6075=VERTEX_POINT('',#20692);
#6076=VERTEX_POINT('',#20696);
#6077=VERTEX_POINT('',#20700);
#7453=EDGE_CURVE('',#6060,#6061,#3623,.T.);
#7454=EDGE_CURVE('',#6061,#6062,#3624,.T.);
#7455=EDGE_CURVE('',#6062,#6063,#3625,.T.);
#7456=EDGE_CURVE('',#6063,#6064,#3626,.T.);
#7457=EDGE_CURVE('',#6064,#6065,#25,.T.);
#7458=EDGE_CURVE('',#6065,#6060,#3627,.T.);
#7459=EDGE_CURVE('',#6066,#6064,#5396,.F.);
#7460=EDGE_CURVE('',#6066,#6067,#3628,.T.);
#7461=EDGE_CURVE('',#6067,#6067,#5397,.T.);
#7462=EDGE_CURVE('',#6068,#6066,#5398,.F.);
#7463=EDGE_CURVE('',#6069,#6068,#26,.T.);
#7464=EDGE_CURVE('',#6065,#6069,#5399,.F.);
#7465=EDGE_CURVE('',#6070,#6063,#3629,.T.);
#7466=EDGE_CURVE('',#6068,#6070,#3630,.T.);
#7467=EDGE_CURVE('',#6071,#6069,#3631,.T.);
#7468=EDGE_CURVE('',#6060,#6071,#3632,.T.);
#7469=EDGE_CURVE('',#6070,#6072,#3633,.T.);
#7470=EDGE_CURVE('',#6072,#6073,#3634,.T.);
#7471=EDGE_CURVE('',#6073,#6071,#3635,.T.);
#7472=EDGE_CURVE('',#6073,#6074,#3636,.T.);
#7473=EDGE_CURVE('',#6075,#6074,#3637,.T.);
#7474=EDGE_CURVE('',#6061,#6075,#3638,.T.);
#7475=EDGE_CURVE('',#6072,#6076,#3639,.T.);
#7476=EDGE_CURVE('',#6074,#6076,#3640,.T.);
#7477=EDGE_CURVE('',#6077,#6075,#3641,.T.);
#7478=EDGE_CURVE('',#6062,#6077,#3642,.T.);
#7479=EDGE_CURVE('',#6076,#6077,#3643,.T.);
#9907=ORIENTED_EDGE('',*,*,#7453,.T.);
#9908=ORIENTED_EDGE('',*,*,#7454,.T.);
#9909=ORIENTED_EDGE('',*,*,#7455,.T.);
#9910=ORIENTED_EDGE('',*,*,#7456,.T.);
#9911=ORIENTED_EDGE('',*,*,#7457,.T.);
#9912=ORIENTED_EDGE('',*,*,#7458,.T.);
#9913=ORIENTED_EDGE('',*,*,#7457,.F.);
#9914=ORIENTED_EDGE('',*,*,#7459,.F.);
#9915=ORIENTED_EDGE('',*,*,#7460,.T.);
#9916=ORIENTED_EDGE('',*,*,#7461,.F.);
#9917=ORIENTED_EDGE('',*,*,#7460,.F.);
#9918=ORIENTED_EDGE('',*,*,#7462,.F.);
#9919=ORIENTED_EDGE('',*,*,#7463,.F.);
#9920=ORIENTED_EDGE('',*,*,#7464,.F.);
#9921=ORIENTED_EDGE('',*,*,#7456,.F.);
#9922=ORIENTED_EDGE('',*,*,#7465,.F.);
#9923=ORIENTED_EDGE('',*,*,#7466,.F.);
#9924=ORIENTED_EDGE('',*,*,#7462,.T.);
#9925=ORIENTED_EDGE('',*,*,#7459,.T.);
#9926=ORIENTED_EDGE('',*,*,#7458,.F.);
#9927=ORIENTED_EDGE('',*,*,#7464,.T.);
#9928=ORIENTED_EDGE('',*,*,#7467,.F.);
#9929=ORIENTED_EDGE('',*,*,#7468,.F.);
#9930=ORIENTED_EDGE('',*,*,#7469,.T.);
#9931=ORIENTED_EDGE('',*,*,#7470,.T.);
#9932=ORIENTED_EDGE('',*,*,#7471,.T.);
#9933=ORIENTED_EDGE('',*,*,#7467,.T.);
#9934=ORIENTED_EDGE('',*,*,#7463,.T.);
#9935=ORIENTED_EDGE('',*,*,#7466,.T.);
#9936=ORIENTED_EDGE('',*,*,#7453,.F.);
#9937=ORIENTED_EDGE('',*,*,#7468,.T.);
#9938=ORIENTED_EDGE('',*,*,#7471,.F.);
#9939=ORIENTED_EDGE('',*,*,#7472,.T.);
#9940=ORIENTED_EDGE('',*,*,#7473,.F.);
#9941=ORIENTED_EDGE('',*,*,#7474,.F.);
#9942=ORIENTED_EDGE('',*,*,#7470,.F.);
#9943=ORIENTED_EDGE('',*,*,#7475,.T.);
#9944=ORIENTED_EDGE('',*,*,#7476,.F.);
#9945=ORIENTED_EDGE('',*,*,#7472,.F.);
#9946=ORIENTED_EDGE('',*,*,#7454,.F.);
#9947=ORIENTED_EDGE('',*,*,#7474,.T.);
#9948=ORIENTED_EDGE('',*,*,#7477,.F.);
#9949=ORIENTED_EDGE('',*,*,#7478,.F.);
#9950=ORIENTED_EDGE('',*,*,#7455,.F.);
#9951=ORIENTED_EDGE('',*,*,#7478,.T.);
#9952=ORIENTED_EDGE('',*,*,#7479,.F.);
#9953=ORIENTED_EDGE('',*,*,#7475,.F.);
#9954=ORIENTED_EDGE('',*,*,#7469,.F.);
#9955=ORIENTED_EDGE('',*,*,#7465,.T.);
#9956=ORIENTED_EDGE('',*,*,#7479,.T.);
#9957=ORIENTED_EDGE('',*,*,#7477,.T.);
#9958=ORIENTED_EDGE('',*,*,#7473,.T.);
#9959=ORIENTED_EDGE('',*,*,#7476,.T.);
#9960=ORIENTED_EDGE('',*,*,#7461,.T.);
#12074=CYLINDRICAL_SURFACE('',#14186,0.2117);
#12586=ADVANCED_FACE('',(#1874),#1390,.T.);
#12587=ADVANCED_FACE('',(#1875),#12074,.F.);
#12588=ADVANCED_FACE('',(#1876),#1391,.F.);
#12589=ADVANCED_FACE('',(#1877),#1392,.F.);
#12590=ADVANCED_FACE('',(#1878),#1393,.T.);
#12591=ADVANCED_FACE('',(#1879),#1394,.T.);
#12592=ADVANCED_FACE('',(#1880),#1395,.T.);
#12593=ADVANCED_FACE('',(#1881),#1396,.T.);
#12594=ADVANCED_FACE('',(#1882),#1397,.T.);
#12595=ADVANCED_FACE('',(#1883,#1148),#1398,.T.);
#13045=CLOSED_SHELL('',(#12586,#12587,#12588,#12589,#12590,#12591,#12592,
#12593,#12594,#12595));
#14183=AXIS2_PLACEMENT_3D('',#20650,#16524,#16525);
#14184=AXIS2_PLACEMENT_3D('',#20651,#16526,#16527);
#14185=AXIS2_PLACEMENT_3D('',#20662,#16532,#16533);
#14186=AXIS2_PLACEMENT_3D('',#20664,#16535,#16536);
#14187=AXIS2_PLACEMENT_3D('',#20666,#16537,#16538);
#14188=AXIS2_PLACEMENT_3D('',#20669,#16540,#16541);
#14189=AXIS2_PLACEMENT_3D('',#20671,#16542,#16543);
#14190=AXIS2_PLACEMENT_3D('',#20673,#16544,#16545);
#14191=AXIS2_PLACEMENT_3D('',#20674,#16546,#16547);
#14192=AXIS2_PLACEMENT_3D('',#20675,#16548,#16549);
#14193=AXIS2_PLACEMENT_3D('',#20679,#16552,#16553);
#14194=AXIS2_PLACEMENT_3D('',#20683,#16556,#16557);
#14195=AXIS2_PLACEMENT_3D('',#20689,#16561,#16562);
#14196=AXIS2_PLACEMENT_3D('',#20695,#16566,#16567);
#14197=AXIS2_PLACEMENT_3D('',#20699,#16570,#16571);
#14198=AXIS2_PLACEMENT_3D('',#20703,#16574,#16575);
#14199=AXIS2_PLACEMENT_3D('',#20705,#16577,#16578);
#16524=DIRECTION('axis',(0.,0.,1.));
#16525=DIRECTION('refdir',(1.,0.,0.));
#16526=DIRECTION('center_axis',(0.,-0.707106781186548,-0.707106781186548));
#16527=DIRECTION('ref_axis',(-1.,0.,0.));
#16528=DIRECTION('',(0.,-0.707106781186548,0.707106781186548));
#16529=DIRECTION('',(-1.,0.,0.));
#16530=DIRECTION('',(0.,0.707106781186548,-0.707106781186548));
#16531=DIRECTION('',(1.,0.,0.));
#16532=DIRECTION('center_axis',(0.,0.707106781186548,0.707106781186548));
#16533=DIRECTION('ref_axis',(0.,0.707106781186547,-0.707106781186547));
#16534=DIRECTION('',(1.,0.,0.));
#16535=DIRECTION('center_axis',(0.,0.,1.));
#16536=DIRECTION('ref_axis',(1.,0.,0.));
#16537=DIRECTION('center_axis',(0.,0.,-1.));
#16538=DIRECTION('ref_axis',(1.,0.,0.));
#16539=DIRECTION('',(0.,0.,1.));
#16540=DIRECTION('center_axis',(0.,0.,-1.));
#16541=DIRECTION('ref_axis',(1.,0.,0.));
#16542=DIRECTION('center_axis',(0.,0.,-1.));
#16543=DIRECTION('ref_axis',(1.,0.,0.));
#16544=DIRECTION('center_axis',(0.,-0.707106781186548,0.707106781186548));
#16545=DIRECTION('ref_axis',(0.,0.707106781186547,0.707106781186547));
#16546=DIRECTION('center_axis',(0.,0.,-1.));
#16547=DIRECTION('ref_axis',(1.,0.,0.));
#16548=DIRECTION('center_axis',(0.,0.,1.));
#16549=DIRECTION('ref_axis',(1.,0.,0.));
#16550=DIRECTION('',(0.,-1.,0.));
#16551=DIRECTION('',(-1.,0.,0.));
#16552=DIRECTION('center_axis',(0.,0.,1.));
#16553=DIRECTION('ref_axis',(1.,0.,0.));
#16554=DIRECTION('',(-1.,0.,0.));
#16555=DIRECTION('',(0.,1.,0.));
#16556=DIRECTION('center_axis',(0.,0.707106781186548,-0.707106781186548));
#16557=DIRECTION('ref_axis',(-1.,0.,0.));
#16558=DIRECTION('',(0.,0.707106781186548,0.707106781186548));
#16559=DIRECTION('',(1.,0.,0.));
#16560=DIRECTION('',(0.,-0.707106781186548,-0.707106781186548));
#16561=DIRECTION('center_axis',(1.,0.,0.));
#16562=DIRECTION('ref_axis',(0.,1.,0.));
#16563=DIRECTION('',(0.,0.,1.));
#16564=DIRECTION('',(0.,1.,0.));
#16565=DIRECTION('',(0.,0.,1.));
#16566=DIRECTION('center_axis',(0.,1.,0.));
#16567=DIRECTION('ref_axis',(-1.,0.,0.));
#16568=DIRECTION('',(0.,0.,1.));
#16569=DIRECTION('',(-1.,0.,0.));
#16570=DIRECTION('center_axis',(0.,-1.,0.));
#16571=DIRECTION('ref_axis',(1.,0.,0.));
#16572=DIRECTION('',(1.,0.,0.));
#16573=DIRECTION('',(0.,0.,1.));
#16574=DIRECTION('center_axis',(-1.,0.,0.));
#16575=DIRECTION('ref_axis',(0.,-1.,0.));
#16576=DIRECTION('',(0.,-1.,0.));
#16577=DIRECTION('center_axis',(0.,0.,1.));
#16578=DIRECTION('ref_axis',(1.,0.,0.));
#20650=CARTESIAN_POINT('',(0.,0.,0.));
#20651=CARTESIAN_POINT('Origin',(-0.25,-0.225,0.075));
#20652=CARTESIAN_POINT('',(0.5,-0.15,0.));
#20653=CARTESIAN_POINT('',(0.5,-0.3,0.15));
#20654=CARTESIAN_POINT('',(0.5,-0.225,0.075));
#20655=CARTESIAN_POINT('',(-0.5,-0.3,0.15));
#20656=CARTESIAN_POINT('',(-0.25,-0.3,0.15));
#20657=CARTESIAN_POINT('',(-0.5,-0.15,0.));
#20658=CARTESIAN_POINT('',(-0.5,-0.075,-0.075));
#20659=CARTESIAN_POINT('',(-0.149388386429468,-0.15,0.));
#20660=CARTESIAN_POINT('',(-0.25,-0.15,0.));
#20661=CARTESIAN_POINT('',(0.149388386429468,-0.15,0.));
#20662=CARTESIAN_POINT('Origin',(0.,0.,-0.15));
#20663=CARTESIAN_POINT('',(-0.25,-0.15,0.));
#20664=CARTESIAN_POINT('Origin',(0.,0.,-0.1));
#20665=CARTESIAN_POINT('',(-0.2117,-2.59257727379495E-17,0.));
#20666=CARTESIAN_POINT('Origin',(0.,0.,0.));
#20667=CARTESIAN_POINT('',(-0.2117,2.59257727379495E-17,0.4));
#20668=CARTESIAN_POINT('',(-0.2117,-2.59257727379495E-17,-0.1));
#20669=CARTESIAN_POINT('Origin',(0.,0.,0.4));
#20670=CARTESIAN_POINT('',(-0.149388386429468,0.15,0.));
#20671=CARTESIAN_POINT('Origin',(0.,0.,0.));
#20672=CARTESIAN_POINT('',(0.149388386429468,0.15,0.));
#20673=CARTESIAN_POINT('Origin',(0.,0.,-0.15));
#20674=CARTESIAN_POINT('Origin',(0.,0.,0.));
#20675=CARTESIAN_POINT('Origin',(0.,0.,0.));
#20676=CARTESIAN_POINT('',(-0.5,0.15,0.));
#20677=CARTESIAN_POINT('',(-0.5,0.3,0.));
#20678=CARTESIAN_POINT('',(0.25,0.15,0.));
#20679=CARTESIAN_POINT('Origin',(0.,0.,0.));
#20680=CARTESIAN_POINT('',(0.5,0.15,0.));
#20681=CARTESIAN_POINT('',(0.25,0.15,0.));
#20682=CARTESIAN_POINT('',(0.5,-0.3,0.));
#20683=CARTESIAN_POINT('Origin',(0.25,0.225,0.075));
#20684=CARTESIAN_POINT('',(-0.5,0.3,0.15));
#20685=CARTESIAN_POINT('',(-0.5,0.225,0.075));
#20686=CARTESIAN_POINT('',(0.5,0.3,0.15));
#20687=CARTESIAN_POINT('',(0.25,0.3,0.15));
#20688=CARTESIAN_POINT('',(0.5,0.075,-0.075));
#20689=CARTESIAN_POINT('Origin',(0.5,-0.3,0.));
#20690=CARTESIAN_POINT('',(0.5,0.3,0.4));
#20691=CARTESIAN_POINT('',(0.5,0.3,0.));
#20692=CARTESIAN_POINT('',(0.5,-0.3,0.4));
#20693=CARTESIAN_POINT('',(0.5,-0.3,0.4));
#20694=CARTESIAN_POINT('',(0.5,-0.3,0.));
#20695=CARTESIAN_POINT('Origin',(0.5,0.3,0.));
#20696=CARTESIAN_POINT('',(-0.5,0.3,0.4));
#20697=CARTESIAN_POINT('',(-0.5,0.3,0.));
#20698=CARTESIAN_POINT('',(0.5,0.3,0.4));
#20699=CARTESIAN_POINT('Origin',(-0.5,-0.3,0.));
#20700=CARTESIAN_POINT('',(-0.5,-0.3,0.4));
#20701=CARTESIAN_POINT('',(-0.5,-0.3,0.4));
#20702=CARTESIAN_POINT('',(-0.5,-0.3,0.));
#20703=CARTESIAN_POINT('Origin',(-0.5,0.3,0.));
#20704=CARTESIAN_POINT('',(-0.5,0.3,0.4));
#20705=CARTESIAN_POINT('Origin',(0.,0.,0.4));
#33902=UNCERTAINTY_MEASURE_WITH_UNIT(LENGTH_MEASURE(0.001),#33982,
'DISTANCE_ACCURACY_VALUE',
'Maximum model space distance between geometric entities at asserted c
onnectivities');
#33929=UNCERTAINTY_MEASURE_WITH_UNIT(LENGTH_MEASURE(0.001),#33982,
'DISTANCE_ACCURACY_VALUE',
'Maximum model space distance between geometric entities at asserted c
onnectivities');
#33954=(
GEOMETRIC_REPRESENTATION_CONTEXT(3)
GLOBAL_UNCERTAINTY_ASSIGNED_CONTEXT((#33902))
GLOBAL_UNIT_ASSIGNED_CONTEXT((#33982,#33984,#33985))
REPRESENTATION_CONTEXT('','3D')
);
#33981=(
GEOMETRIC_REPRESENTATION_CONTEXT(3)
GLOBAL_UNCERTAINTY_ASSIGNED_CONTEXT((#33929))
GLOBAL_UNIT_ASSIGNED_CONTEXT((#33982,#33984,#33985))
REPRESENTATION_CONTEXT('','3D')
);
#33982=(
LENGTH_UNIT()
NAMED_UNIT(*)
SI_UNIT(.CENTI.,.METRE.)
);
#33984=(
NAMED_UNIT(*)
PLANE_ANGLE_UNIT()
SI_UNIT($,.RADIAN.)
);
#33985=(
NAMED_UNIT(*)
SI_UNIT($,.STERADIAN.)
SOLID_ANGLE_UNIT()
);
#34010=SHAPE_DEFINITION_REPRESENTATION(#34071,#34206);
#34071=PRODUCT_DEFINITION_SHAPE('',$,#34258);
#34206=SHAPE_REPRESENTATION('',(#14183),#33954);
#34233=PRODUCT_DEFINITION_CONTEXT('part definition',#34388,'design');
#34258=PRODUCT_DEFINITION('Slot Nut - M5 for 20 mm Extrusion',
'Slot Nut - M5 for 20 mm Extrusion',#34309,#34233);
#34309=PRODUCT_DEFINITION_FORMATION('',$,#34414);
#34388=APPLICATION_CONTEXT(
'Core Data for Automotive Mechanical Design Process');
#34389=PRODUCT_CONTEXT('part definition',#34388,'mechanical');
#34414=PRODUCT('Slot Nut - M5 for 20 mm Extrusion',
'Slot Nut - M5 for 20 mm Extrusion','Slot Nut - M5 for 20 mm Extrusion',
(#34389));
#34518=COLOUR_RGB('Black',0.12,0.14,0.17);
#34519=FILL_AREA_STYLE_COLOUR('',#34518);
#34520=FILL_AREA_STYLE('',(#34519));
#34521=SURFACE_STYLE_FILL_AREA(#34520);
#34522=SURFACE_SIDE_STYLE('',(#34521));
#34523=SURFACE_STYLE_USAGE(.BOTH.,#34522);
#34524=PRESENTATION_STYLE_ASSIGNMENT((#34523));
ENDSEC;
END-ISO-10303-21;
